ISO-10303-21;
HEADER;
FILE_DESCRIPTION (('STEP AP214'),
    '1' );
FILE_NAME ('Screw 5.step',
    '2026-10-26T17:37:43',
    ( '' ),
    ( '' ),
    'SwSTEP 2.0',
    'SolidWorks 2024',
    '' );
FILE_SCHEMA (( 'AUTOMOTIVE_DESIGN' ));
ENDSEC;

DATA;
#16=FACE_OUTER_BOUND ( 'NONE', #5974, .T. ) ;
#33=CARTESIAN_POINT ( 'NONE',  ( 139.6999999999999886, -3574.034000000000106, 2239.391000000000076 ) ) ;
#46=DIRECTION ( 'NONE',  ( 0.000000000000000000, 0.000000000000000000, -1.000000000000000000 ) ) ;
#86=AXIS2_PLACEMENT_3D ( 'NONE', #9991, #1078, #11873 ) ;
#118=VERTEX_POINT ( 'NONE', #15723 ) ;
#184=AXIS2_PLACEMENT_3D ( 'NONE', #20222, #9553, #4165 ) ;
#189=DIRECTION ( 'NONE',  ( 0.000000000000000000, 1.000000000000000000, 0.000000000000000000 ) ) ;
#232=PLANE ( 'NONE',  #19911 ) ;
#245=CARTESIAN_POINT ( 'NONE',  ( 142.0316867971999955, -3578.148799999999937, 2242.820000000000164 ) ) ;
#247=DIRECTION ( 'NONE',  ( -1.000000000000000000, -1.165588477296775430E-12, 0.000000000000000000 ) ) ;
#308=CARTESIAN_POINT ( 'NONE',  ( 139.6999999999999886, -3579.494999999999891, 2270.760000000000218 ) ) ;
#309=VERTEX_POINT ( 'NONE', #12898 ) ;
#343=EDGE_CURVE ( 'NONE', #1907, #13051, #5539, .T. ) ;
#361=ORIENTED_EDGE ( 'NONE', *, *, #15519, .F. ) ;
#395=FACE_OUTER_BOUND ( 'NONE', #15654, .T. ) ;
#452=VERTEX_POINT ( 'NONE', #1504 ) ;
#470=ORIENTED_EDGE ( 'NONE', *, *, #12681, .F. ) ;
#493=FACE_OUTER_BOUND ( 'NONE', #11392, .T. ) ;
#496=AXIS2_PLACEMENT_3D ( 'NONE', #13817, #20958, #9934 ) ;
#503=EDGE_CURVE ( 'NONE', #4557, #452, #5825, .T. ) ;
#512=CIRCLE ( 'NONE', #14369, 0.3809999999999647002 ) ;
#519=VECTOR ( 'NONE', #3642, 1000.000000000000000 ) ;
#570=PRODUCT_DEFINITION_CONTEXT ( 'detailed design', #18003, 'design' ) ;
#606=DIRECTION ( 'NONE',  ( -2.324635735433000053E-14, 2.336881798971000105E-14, -1.000000000000000000 ) ) ;
#631=EDGE_CURVE ( 'NONE', #20297, #452, #17568, .T. ) ;
#646=PLANE ( 'NONE',  #2051 ) ;
#668=ORIENTED_EDGE ( 'NONE', *, *, #15029, .F. ) ;
#717=LINE ( 'NONE', #21821, #6652 ) ;
#761=DIRECTION ( 'NONE',  ( 1.224646799141920914E-16, -1.000000000000000000, -2.336881798971000421E-14 ) ) ;
#777=DIRECTION ( 'NONE',  ( 0.000000000000000000, 1.000000000000000000, 0.000000000000000000 ) ) ;
#812=EDGE_LOOP ( 'NONE', ( #1054, #19308, #16094, #2835 ) ) ;
#839=ORIENTED_EDGE ( 'NONE', *, *, #631, .T. ) ;
#890=DIRECTION ( 'NONE',  ( 0.000000000000000000, -1.000000000000000000, 0.000000000000000000 ) ) ;
#897=CARTESIAN_POINT ( 'NONE',  ( 137.3683132029016178, -3580.841200000194931, 2239.167815367238745 ) ) ;
#907=CIRCLE ( 'NONE', #20759, 3.175000000000149925 ) ;
#954=CARTESIAN_POINT ( 'NONE',  ( 139.6999999999999886, -3579.494999999999891, 2272.030000000000200 ) ) ;
#959=DIRECTION ( 'NONE',  ( 0.000000000000000000, -2.336881798971000105E-14, 1.000000000000000000 ) ) ;
#983=CARTESIAN_POINT ( 'NONE',  ( 139.7000000000063835, -3576.802599999822633, 2239.167815367340609 ) ) ;
#996=DIRECTION ( 'NONE',  ( 0.000000000000000000, 0.000000000000000000, -1.000000000000000000 ) ) ;
#1017=ORIENTED_EDGE ( 'NONE', *, *, #3853, .F. ) ;
#1020=DIRECTION ( 'NONE',  ( 0.8660254037820785955, -0.5000000000040877302, -3.181634500919918361E-14 ) ) ;
#1032=CARTESIAN_POINT ( 'NONE',  ( 134.6199999999999761, -3579.494999999999891, 2239.009999999999764 ) ) ;
#1054=ORIENTED_EDGE ( 'NONE', *, *, #11441, .T. ) ;
#1062=ORIENTED_EDGE ( 'NONE', *, *, #14592, .T. ) ;
#1067=CARTESIAN_POINT ( 'NONE',  ( 139.6999999999999886, -3579.494999999999891, 2245.359999999999673 ) ) ;
#1078=DIRECTION ( 'NONE',  ( -2.324635735433000053E-14, 0.000000000000000000, -1.000000000000000000 ) ) ;
#1080=EDGE_CURVE ( 'NONE', #9518, #22946, #12776, .T. ) ;
#1116=EDGE_CURVE ( 'NONE', #20178, #4557, #4253, .T. ) ;
#1126=ADVANCED_FACE ( 'NONE', ( #2713 ), #22166, .F. ) ;
#1171=AXIS2_PLACEMENT_3D ( 'NONE', #4369, #8003, #15148 ) ;
#1187=LINE ( 'NONE', #6483, #14984 ) ;
#1191=EDGE_CURVE ( 'NONE', #6461, #15432, #8756, .T. ) ;
#1204=ADVANCED_FACE ( 'NONE', ( #13742 ), #20887, .T. ) ;
#1232=VERTEX_POINT ( 'NONE', #15961 ) ;
#1303=CARTESIAN_POINT ( 'NONE',  ( 139.6999999999985675, -3582.369629489782255, 2239.009999999944739 ) ) ;
#1323=ORIENTED_EDGE ( 'NONE', *, *, #19679, .F. ) ;
#1329=EDGE_CURVE ( 'NONE', #2593, #18880, #9040, .T. ) ;
#1354=VECTOR ( 'NONE', #5449, 1000.000000000000000 ) ;
#1359=DIRECTION ( 'NONE',  ( 0.000000000000000000, -1.000000000000000000, 0.000000000000000000 ) ) ;
#1492=FACE_OUTER_BOUND ( 'NONE', #22547, .T. ) ;
#1504=CARTESIAN_POINT ( 'NONE',  ( 139.7000000000063835, -3576.802599999938593, 2239.391000000000076 ) ) ;
#1506=ORIENTED_EDGE ( 'NONE', *, *, #17845, .T. ) ;
#1540=EDGE_CURVE ( 'NONE', #13123, #14851, #5320, .T. ) ;
#1559=ORIENTED_EDGE ( 'NONE', *, *, #3188, .F. ) ;
#1597=CARTESIAN_POINT ( 'NONE',  ( 134.2390000000000043, -3579.494999999999891, 2244.978999999999814 ) ) ;
#1603=DIRECTION ( 'NONE',  ( 1.000000000000000000, 5.432398939370942693E-28, -2.324635735433000053E-14 ) ) ;
#1651=DIRECTION ( 'NONE',  ( 0.5000000000040877302, 0.8660254037820785955, 0.000000000000000000 ) ) ;
#1718=ADVANCED_FACE ( 'NONE', ( #21669 ), #232, .T. ) ;
#1799=ADVANCED_FACE ( 'NONE', ( #5624 ), #20640, .T. ) ;
#1809=VERTEX_POINT ( 'NONE', #12760 ) ;
#1810=LINE ( 'NONE', #18092, #1354 ) ;
#1831=ADVANCED_FACE ( 'NONE', ( #14642 ), #18048, .T. ) ;
#1867=ORIENTED_EDGE ( 'NONE', *, *, #22414, .T. ) ;
#1907=VERTEX_POINT ( 'NONE', #15209 ) ;
#1931=SHAPE_DEFINITION_REPRESENTATION ( #19683, #21348 ) ;
#1938=EDGE_LOOP ( 'NONE', ( #1559, #5914, #14362, #3986 ) ) ;
#1948=EDGE_LOOP ( 'NONE', ( #13258, #3240, #10560, #10064 ) ) ;
#1955=AXIS2_PLACEMENT_3D ( 'NONE', #6196, #1020, #11459 ) ;
#1966=LINE ( 'NONE', #7469, #16553 ) ;
#2021=EDGE_LOOP ( 'NONE', ( #17301, #1062 ) ) ;
#2035=ORIENTED_EDGE ( 'NONE', *, *, #503, .F. ) ;
#2039=CYLINDRICAL_SURFACE ( 'NONE', #5814, 0.3809999999999924558 ) ;
#2042=CARTESIAN_POINT ( 'NONE',  ( 142.4126867972000241, -3577.928829547000078, 2239.009999999999764 ) ) ;
#2047=DIRECTION ( 'NONE',  ( 0.000000000000000000, -1.000000000000000000, 0.000000000000000000 ) ) ;
#2051=AXIS2_PLACEMENT_3D ( 'NONE', #22075, #2404, #16693 ) ;
#2053=ORIENTED_EDGE ( 'NONE', *, *, #22020, .T. ) ;
#2089=CIRCLE ( 'NONE', #15918, 3.175000000000149925 ) ;
#2153=ORIENTED_EDGE ( 'NONE', *, *, #20313, .T. ) ;
#2178=FACE_OUTER_BOUND ( 'NONE', #3662, .T. ) ;
#2194=CARTESIAN_POINT ( 'NONE',  ( 142.0316867971391162, -3578.148799999964467, 2239.391000000000076 ) ) ;
#2257=( GEOMETRIC_REPRESENTATION_CONTEXT ( 3 ) GLOBAL_UNCERTAINTY_ASSIGNED_CONTEXT ( ( #16741 ) ) GLOBAL_UNIT_ASSIGNED_CONTEXT ( ( #21126, #3419, #23094 ) ) REPRESENTATION_CONTEXT ( 'NONE', 'WORKASPACE' ) );
#2298=CARTESIAN_POINT ( 'NONE',  ( 139.6999999999999886, -3579.494999999999891, 2270.760000000000218 ) ) ;
#2319=( BOUNDED_CURVE ( )  B_SPLINE_CURVE ( 3, ( #15784, #21297, #3005, #4879 ),
 .UNSPECIFIED., .F., .T. ) 
 B_SPLINE_CURVE_WITH_KNOTS ( ( 4, 4 ),
 ( -2.664535259100375697E-14, 1.570796326191299608 ),
 .UNSPECIFIED. ) 
 CURVE ( )  GEOMETRIC_REPRESENTATION_ITEM ( )  RATIONAL_B_SPLINE_CURVE ( ( 1.000000000000000000, 0.8047378542666279166, 0.8047378542666279166, 1.000000000000000000 ) ) 
 REPRESENTATION_ITEM ( '' )  );
#2369=CARTESIAN_POINT ( 'NONE',  ( 136.9873132028999976, -3581.061170452877832, 2239.009999999999764 ) ) ;
#2404=DIRECTION ( 'NONE',  ( 0.000000000000000000, 0.000000000000000000, -1.000000000000000000 ) ) ;
#2422=VECTOR ( 'NONE', #4283, 1000.000000000000000 ) ;
#2499=CARTESIAN_POINT ( 'NONE',  ( 142.0316867971999955, -3580.841199999999844, 2239.391000000000076 ) ) ;
#2543=CARTESIAN_POINT ( 'NONE',  ( 136.9873132028999976, -3581.061170452999704, 2239.009999999999764 ) ) ;
#2570=CARTESIAN_POINT ( 'NONE',  ( 139.6999999999999886, -3582.187399999999798, 2239.391000000000076 ) ) ;
#2593=VERTEX_POINT ( 'NONE', #22858 ) ;
#2606=CARTESIAN_POINT ( 'NONE',  ( 0.000000000000000000, 0.000000000000000000, 0.000000000000000000 ) ) ;
#2672=CYLINDRICAL_SURFACE ( 'NONE', #9830, 0.3810000000000330345 ) ;
#2713=FACE_OUTER_BOUND ( 'NONE', #13101, .T. ) ;
#2731=ORIENTED_EDGE ( 'NONE', *, *, #16718, .T. ) ;
#2742=VECTOR ( 'NONE', #3932, 999.9999999999998863 ) ;
#2778=VERTEX_POINT ( 'NONE', #17103 ) ;
#2835=ORIENTED_EDGE ( 'NONE', *, *, #15310, .F. ) ;
#3005=CARTESIAN_POINT ( 'NONE',  ( 137.2104978357572236, -3578.057685255099841, 2239.010000000134823 ) ) ;
#3059=CARTESIAN_POINT ( 'NONE',  ( 139.6999999999999886, -3576.320000000000164, 2270.760000000000218 ) ) ;
#3064=CIRCLE ( 'NONE', #86, 5.460999999999938126 ) ;
#3128=AXIS2_PLACEMENT_3D ( 'NONE', #17547, #9324, #5025 ) ;
#3172=VECTOR ( 'NONE', #3517, 1000.000000000000000 ) ;
#3188=EDGE_CURVE ( 'NONE', #1907, #22946, #15631, .T. ) ;
#3196=VECTOR ( 'NONE', #7032, 1000.000000000000000 ) ;
#3240=ORIENTED_EDGE ( 'NONE', *, *, #13995, .T. ) ;
#3317=DIRECTION ( 'NONE',  ( -2.324635735433000053E-14, 2.336881798971000105E-14, -1.000000000000000000 ) ) ;
#3351=CARTESIAN_POINT ( 'NONE',  ( 136.9873132028999976, -3581.061170452999704, 2239.009999999999764 ) ) ;
#3385=CIRCLE ( 'NONE', #12745, 5.080000000000000959 ) ;
#3395=DIRECTION ( 'NONE',  ( -3.156802126040999989E-13, 2.590196616237999979E-13, -1.000000000000000000 ) ) ;
#3419=( NAMED_UNIT ( * ) PLANE_ANGLE_UNIT ( ) SI_UNIT ( $, .RADIAN. ) );
#3517=DIRECTION ( 'NONE',  ( 0.000000000000000000, 0.000000000000000000, -1.000000000000000000 ) ) ;
#3557=CARTESIAN_POINT ( 'NONE',  ( 142.4126867972000241, -3579.494999999999891, 2239.391000000000076 ) ) ;
#3571=DIRECTION ( 'NONE',  ( 0.000000000000000000, 0.000000000000000000, -1.000000000000000000 ) ) ;
#3615=CARTESIAN_POINT ( 'NONE',  ( 137.3683132029851208, -3580.841200000048957, 2239.391000000000076 ) ) ;
#3636=EDGE_CURVE ( 'NONE', #3840, #22617, #17949, .T. ) ;
#3642=DIRECTION ( 'NONE',  ( 0.000000000000000000, 0.000000000000000000, -1.000000000000000000 ) ) ;
#3662=EDGE_LOOP ( 'NONE', ( #14176, #11005 ) ) ;
#3667=ORIENTED_EDGE ( 'NONE', *, *, #1191, .F. ) ;
#3685=VERTEX_POINT ( 'NONE', #33 ) ;
#3696=DIRECTION ( 'NONE',  ( 0.000000000000000000, 0.000000000000000000, -1.000000000000000000 ) ) ;
#3799=EDGE_CURVE ( 'NONE', #2593, #17406, #717, .T. ) ;
#3828=DIRECTION ( 'NONE',  ( 1.000000000000000000, 0.000000000000000000, 0.000000000000000000 ) ) ;
#3829=DIRECTION ( 'NONE',  ( -0.8660254037840939834, -0.5000000000005969669, 0.000000000000000000 ) ) ;
#3832=FACE_OUTER_BOUND ( 'NONE', #22772, .T. ) ;
#3840=VERTEX_POINT ( 'NONE', #9404 ) ;
#3853=EDGE_CURVE ( 'NONE', #11610, #17406, #21930, .T. ) ;
#3892=VERTEX_POINT ( 'NONE', #2369 ) ;
#3912=LINE ( 'NONE', #2042, #17444 ) ;
#3923=DIRECTION ( 'NONE',  ( 0.000000000000000000, -1.000000000000000000, 0.000000000000000000 ) ) ;
#3932=DIRECTION ( 'NONE',  ( -0.8660254037817188832, 0.5000000000047110094, 0.000000000000000000 ) ) ;
#3986=ORIENTED_EDGE ( 'NONE', *, *, #21004, .F. ) ;
#4074=CIRCLE ( 'NONE', #16792, 5.460999999999938126 ) ;
#4088=UNCERTAINTY_MEASURE_WITH_UNIT (LENGTH_MEASURE( 1.000000000000000082E-05 ), #16644, 'distance_accuracy_value', 'NONE');
#4115=( NAMED_UNIT ( * ) PLANE_ANGLE_UNIT ( ) SI_UNIT ( $, .RADIAN. ) );
#4165=DIRECTION ( 'NONE',  ( 0.5000000000047859494, 0.8660254037816754735, 0.000000000000000000 ) ) ;
#4209=AXIS2_PLACEMENT_3D ( 'NONE', #17654, #15792, #1603 ) ;
#4227=EDGE_CURVE ( 'NONE', #22617, #4557, #10894, .T. ) ;
#4250=ORIENTED_EDGE ( 'NONE', *, *, #17246, .F. ) ;
#4251=CARTESIAN_POINT ( 'NONE',  ( 139.6999999999999886, -3579.494999999999891, 2272.030000000000200 ) ) ;
#4253=LINE ( 'NONE', #2499, #13903 ) ;
#4259=DIRECTION ( 'NONE',  ( 0.000000000000000000, -1.000000000000000000, 0.000000000000000000 ) ) ;
#4283=DIRECTION ( 'NONE',  ( 0.8660254037822586737, -0.5000000000037757575, 0.000000000000000000 ) ) ;
#4292=AXIS2_PLACEMENT_3D ( 'NONE', #5882, #11361, #11142 ) ;
#4317=PLANE ( 'NONE',  #6095 ) ;
#4339=ORIENTED_EDGE ( 'NONE', *, *, #22414, .F. ) ;
#4369=CARTESIAN_POINT ( 'NONE',  ( 142.0316867971999955, -3575.456400000000031, 2242.820000000000164 ) ) ;
#4422=ORIENTED_EDGE ( 'NONE', *, *, #19679, .T. ) ;
#4440=DIRECTION ( 'NONE',  ( 0.5000000000031885605, -0.8660254037825977358, 0.000000000000000000 ) ) ;
#4460=DIRECTION ( 'NONE',  ( -0.8660254037821902839, 0.5000000000038942183, 1.814359422184980810E-12 ) ) ;
#4478=CARTESIAN_POINT ( 'NONE',  ( 139.6999999999999886, -3579.494999999999891, 2245.359999999999673 ) ) ;
#4551=AXIS2_PLACEMENT_3D ( 'NONE', #11588, #9497, #8093 ) ;
#4556=VERTEX_POINT ( 'NONE', #10521 ) ;
#4557=VERTEX_POINT ( 'NONE', #19319 ) ;
#4590=DIRECTION ( 'NONE',  ( 0.000000000000000000, 1.000000000000000000, 0.000000000000000000 ) ) ;
#4654=DIRECTION ( 'NONE',  ( -0.5000000000047110094, -0.8660254037817188832, 0.000000000000000000 ) ) ;
#4666=AXIS2_PLACEMENT_3D ( 'NONE', #16216, #12929, #11177 ) ;
#4670=ADVANCED_FACE ( 'NONE', ( #3832 ), #20018, .T. ) ;
#4671=DIRECTION ( 'NONE',  ( 0.8660254037827048723, 0.5000000000030029312, 0.000000000000000000 ) ) ;
#4761=CARTESIAN_POINT ( 'NONE',  ( 139.6999999999999886, -3579.494999999999891, 2270.760000000000218 ) ) ;
#4879=CARTESIAN_POINT ( 'NONE',  ( 136.9873132030508600, -3577.928829547506666, 2239.009999999999764 ) ) ;
#4916=ORIENTED_EDGE ( 'NONE', *, *, #21056, .T. ) ;
#4964=ORIENTED_EDGE ( 'NONE', *, *, #17246, .T. ) ;
#5025=DIRECTION ( 'NONE',  ( -1.000000000000000000, 0.000000000000000000, 2.324635735433000053E-14 ) ) ;
#5027=ORIENTED_EDGE ( 'NONE', *, *, #11548, .T. ) ;
#5141=DIRECTION ( 'NONE',  ( 1.000000000000000000, 5.432398939370942693E-28, -2.324635735433000053E-14 ) ) ;
#5190=ORIENTED_EDGE ( 'NONE', *, *, #10783, .T. ) ;
#5205=ORIENTED_EDGE ( 'NONE', *, *, #21004, .T. ) ;
#5256=CARTESIAN_POINT ( 'NONE',  ( 139.6999999999999886, -3579.494999999999891, 2244.978999999999814 ) ) ;
#5285=DIRECTION ( 'NONE',  ( 5.432398939370942693E-28, 1.000000000000000000, 2.336881798971000105E-14 ) ) ;
#5291=DIRECTION ( 'NONE',  ( -0.5000000000007168710, 0.8660254037840248165, 0.000000000000000000 ) ) ;
#5320=CIRCLE ( 'NONE', #4551, 0.3809999999999647002 ) ;
#5352=CYLINDRICAL_SURFACE ( 'NONE', #11770, 3.175000000000149925 ) ;
#5406=EDGE_CURVE ( 'NONE', #13051, #22822, #10025, .T. ) ;
#5416=AXIS2_PLACEMENT_3D ( 'NONE', #4761, #10613, #12265 ) ;
#5449=DIRECTION ( 'NONE',  ( -4.128125857118000170E-13, 1.295098308114999897E-13, 1.000000000000000000 ) ) ;
#5539=LINE ( 'NONE', #12781, #519 ) ;
#5545=ADVANCED_FACE ( 'NONE', ( #9146 ), #9264, .T. ) ;
#5611=AXIS2_PLACEMENT_3D ( 'NONE', #2606, #9751, #7545 ) ;
#5624=FACE_OUTER_BOUND ( 'NONE', #1938, .T. ) ;
#5634=AXIS2_PLACEMENT_3D ( 'NONE', #18589, #13084, #14962 ) ;
#5744=CARTESIAN_POINT ( 'NONE',  ( 139.6999999999999886, -3579.494999999999891, 2244.978999999999814 ) ) ;
#5752=EDGE_CURVE ( 'NONE', #18880, #452, #11932, .T. ) ;
#5755=FACE_OUTER_BOUND ( 'NONE', #2021, .T. ) ;
#5814=AXIS2_PLACEMENT_3D ( 'NONE', #3557, #10712, #15268 ) ;
#5825=LINE ( 'NONE', #12842, #2742 ) ;
#5843=ADVANCED_FACE ( 'NONE', ( #1492 ), #10634, .T. ) ;
#5850=ORIENTED_EDGE ( 'NONE', *, *, #3636, .F. ) ;
#5857=ORIENTED_EDGE ( 'NONE', *, *, #7508, .F. ) ;
#5882=CARTESIAN_POINT ( 'NONE',  ( 139.6999999999999886, -3579.494999999999891, 2239.391000000000076 ) ) ;
#5914=ORIENTED_EDGE ( 'NONE', *, *, #20169, .T. ) ;
#5940=CYLINDRICAL_SURFACE ( 'NONE', #184, 0.3809999999999260090 ) ;
#5971=CARTESIAN_POINT ( 'NONE',  ( 137.3683132029851208, -3580.841200000048957, 2239.391000000000076 ) ) ;
#5974=EDGE_LOOP ( 'NONE', ( #21258, #19490, #21220, #839 ) ) ;
#6011=LINE ( 'NONE', #11272, #17306 ) ;
#6041=AXIS2_PLACEMENT_3D ( 'NONE', #18352, #761, #996 ) ;
#6095=AXIS2_PLACEMENT_3D ( 'NONE', #13567, #4654, #18379 ) ;
#6190=ORIENTED_EDGE ( 'NONE', *, *, #5406, .T. ) ;
#6196=CARTESIAN_POINT ( 'NONE',  ( 138.3436566013999993, -3581.844255679000071, 2239.391000000000076 ) ) ;
#6208=CARTESIAN_POINT ( 'NONE',  ( 142.0316867971268096, -3580.841200000091249, 2239.391000000000076 ) ) ;
#6326=CARTESIAN_POINT ( 'NONE',  ( 141.0563433985999779, -3581.844255679000071, 2239.391000000000076 ) ) ;
#6336=ORIENTED_EDGE ( 'NONE', *, *, #1116, .F. ) ;
#6370=CYLINDRICAL_SURFACE ( 'NONE', #18078, 5.460999999999938126 ) ;
#6386=ORIENTED_EDGE ( 'NONE', *, *, #7568, .T. ) ;
#6408=ADVANCED_FACE ( 'NONE', ( #16351 ), #19871, .T. ) ;
#6430=FACE_OUTER_BOUND ( 'NONE', #8159, .T. ) ;
#6461=VERTEX_POINT ( 'NONE', #14829 ) ;
#6483=CARTESIAN_POINT ( 'NONE',  ( 139.7000000001000046, -3576.802599999999984, 2242.820000000000164 ) ) ;
#6534=CARTESIAN_POINT ( 'NONE',  ( 139.6999999999999886, -3579.494999999999891, 2239.391000000000076 ) ) ;
#6603=ORIENTED_EDGE ( 'NONE', *, *, #16122, .T. ) ;
#6604=CARTESIAN_POINT ( 'NONE',  ( 139.6999999999986528, -3582.187400000082107, 2239.391000000000076 ) ) ;
#6611=AXIS2_PLACEMENT_3D ( 'NONE', #17498, #3317, #17731 ) ;
#6652=VECTOR ( 'NONE', #20181, 1000.000000000000000 ) ;
#6653=CARTESIAN_POINT ( 'NONE',  ( 139.7000000001000046, -3576.802599999999984, 2242.820000000000164 ) ) ;
#6733=VERTEX_POINT ( 'NONE', #12580 ) ;
#6854=FACE_OUTER_BOUND ( 'NONE', #15933, .T. ) ;
#6879=FACE_OUTER_BOUND ( 'NONE', #7974, .T. ) ;
#6887=CARTESIAN_POINT ( 'NONE',  ( 139.7000000002929596, -3576.362659094888386, 2239.009999999999764 ) ) ;
#6928=CARTESIAN_POINT ( 'NONE',  ( 136.9873132028999976, -3579.494999999999891, 2239.391000000000076 ) ) ;
#6994=EDGE_LOOP ( 'NONE', ( #4250, #22819, #16162, #7187, #14132, #16639 ) ) ;
#7032=DIRECTION ( 'NONE',  ( 1.710167014410999932E-12, -1.000000000000000000, 0.000000000000000000 ) ) ;
#7145=DIRECTION ( 'NONE',  ( 0.000000000000000000, 0.000000000000000000, 1.000000000000000000 ) ) ;
#7157=DIRECTION ( 'NONE',  ( -1.000000000000000000, 0.000000000000000000, 2.324635735433000053E-14 ) ) ;
#7187=ORIENTED_EDGE ( 'NONE', *, *, #11514, .T. ) ;
#7238=ORIENTED_EDGE ( 'NONE', *, *, #10577, .T. ) ;
#7249=CARTESIAN_POINT ( 'NONE',  ( 139.7000000001000046, -3576.802599999999984, 2242.820000000000164 ) ) ;
#7372=ORIENTED_EDGE ( 'NONE', *, *, #1329, .T. ) ;
#7469=CARTESIAN_POINT ( 'NONE',  ( 139.6999999999999886, -3582.627340905000437, 2239.009999999999764 ) ) ;
#7508=EDGE_CURVE ( 'NONE', #15124, #11974, #3385, .T. ) ;
#7545=DIRECTION ( 'NONE',  ( 1.000000000000000000, 0.000000000000000000, 0.000000000000000000 ) ) ;
#7568=EDGE_CURVE ( 'NONE', #18880, #22617, #1187, .T. ) ;
#7598=CIRCLE ( 'NONE', #496, 5.460999999999938126 ) ;
#7620=CARTESIAN_POINT ( 'NONE',  ( 137.3683132029000262, -3578.148799999999937, 2242.820000000000164 ) ) ;
#7790=ORIENTED_EDGE ( 'NONE', *, *, #21135, .F. ) ;
#7803=CARTESIAN_POINT ( 'NONE',  ( 137.3683132029000262, -3580.841199999999844, 2239.391000000000076 ) ) ;
#7822=DIRECTION ( 'NONE',  ( -1.000000000000000000, 1.224646799147353207E-16, 0.000000000000000000 ) ) ;
#7832=ORIENTED_EDGE ( 'NONE', *, *, #4227, .T. ) ;
#7906=CARTESIAN_POINT ( 'NONE',  ( 139.6999999999999886, -3582.187399999999798, 2242.820000000000164 ) ) ;
#7908=AXIS2_PLACEMENT_3D ( 'NONE', #954, #15037, #4590 ) ;
#7919=EDGE_LOOP ( 'NONE', ( #6190, #11906 ) ) ;
#7974=EDGE_LOOP ( 'NONE', ( #11051, #11857, #16273, #7790 ) ) ;
#8003=DIRECTION ( 'NONE',  ( -2.903809793931999834E-13, 4.457650181899999573E-12, 1.000000000000000000 ) ) ;
#8007=ORIENTED_EDGE ( 'NONE', *, *, #11441, .F. ) ;
#8010=DIRECTION ( 'NONE',  ( -1.000000000000000000, 0.000000000000000000, 0.000000000000000000 ) ) ;
#8037=CIRCLE ( 'NONE', #4292, 5.460999999999938126 ) ;
#8042=ORIENTED_EDGE ( 'NONE', *, *, #7568, .F. ) ;
#8093=DIRECTION ( 'NONE',  ( 0.000000000000000000, 0.000000000000000000, 1.000000000000000000 ) ) ;
#8159=EDGE_LOOP ( 'NONE', ( #2035, #9298, #8042, #9055 ) ) ;
#8266=EDGE_LOOP ( 'NONE', ( #18650, #7238, #2053, #19593, #9281, #10042 ) ) ;
#8282=CARTESIAN_POINT ( 'NONE',  ( 139.6999999999999886, -3579.494999999999891, 2270.760000000000218 ) ) ;
#8315=CARTESIAN_POINT ( 'NONE',  ( 134.6199999999999761, -3579.494999999999891, 2245.359999999999673 ) ) ;
#8327=TOROIDAL_SURFACE ( 'NONE', #4209, 5.080000000000000071, 0.3810000000000000053 ) ;
#8329=AXIS2_PLACEMENT_3D ( 'NONE', #20182, #606, #5141 ) ;
#8364=AXIS2_PLACEMENT_3D ( 'NONE', #17014, #959, #8010 ) ;
#8389=CARTESIAN_POINT ( 'NONE',  ( 139.6999999999999886, -3579.494999999999891, 2245.359999999999673 ) ) ;
#8393=AXIS2_PLACEMENT_3D ( 'NONE', #23142, #8755, #10504 ) ;
#8487=ORIENTED_EDGE ( 'NONE', *, *, #3853, .T. ) ;
#8514=EDGE_LOOP ( 'NONE', ( #8007, #18376, #21619, #16421 ) ) ;
#8585=DIRECTION ( 'NONE',  ( -1.000000000000000000, 0.000000000000000000, 0.000000000000000000 ) ) ;
#8727=CARTESIAN_POINT ( 'NONE',  ( 139.7000000000001876, -3582.670000000000073, 2245.359999999999673 ) ) ;
#8755=DIRECTION ( 'NONE',  ( 0.000000000000000000, 2.336881798971000105E-14, -1.000000000000000000 ) ) ;
#8756=( BOUNDED_CURVE ( )  B_SPLINE_CURVE ( 3, ( #6604, #22626, #1303, #22747 ),
 .UNSPECIFIED., .F., .F. ) 
 B_SPLINE_CURVE_WITH_KNOTS ( ( 4, 4 ),
 ( 3.673835071120113713E-14, 1.570796327042234264 ),
 .UNSPECIFIED. ) 
 CURVE ( )  GEOMETRIC_REPRESENTATION_ITEM ( )  RATIONAL_B_SPLINE_CURVE ( ( 1.000000000000000000, 0.8047378540660755641, 0.8047378540660755641, 1.000000000000000000 ) ) 
 REPRESENTATION_ITEM ( '' )  );
#8770=DIRECTION ( 'NONE',  ( 0.5000000000005969669, -0.8660254037840939834, 0.000000000000000000 ) ) ;
#8868=DIRECTION ( 'NONE',  ( -1.125343061319999876E-12, 1.000000000000000000, 0.000000000000000000 ) ) ;
#8894=LINE ( 'NONE', #17437, #3196 ) ;
#8897=ORIENTED_EDGE ( 'NONE', *, *, #13215, .T. ) ;
#8910=DIRECTION ( 'NONE',  ( -2.324635735433000053E-14, 2.336881798971000105E-14, -1.000000000000000000 ) ) ;
#8995=DIRECTION ( 'NONE',  ( 0.8660254037825501072, 0.5000000000032710501, 0.000000000000000000 ) ) ;
#9016=DIRECTION ( 'NONE',  ( 1.000000000000000000, 5.432398939370942693E-28, -2.324635735433000053E-14 ) ) ;
#9040=LINE ( 'NONE', #7620, #9049 ) ;
#9042=ORIENTED_EDGE ( 'NONE', *, *, #5752, .F. ) ;
#9049=VECTOR ( 'NONE', #9159, 1000.000000000000114 ) ;
#9055=ORIENTED_EDGE ( 'NONE', *, *, #5752, .T. ) ;
#9097=DIRECTION ( 'NONE',  ( 0.000000000000000000, 0.000000000000000000, -1.000000000000000000 ) ) ;
#9146=FACE_OUTER_BOUND ( 'NONE', #14252, .T. ) ;
#9159=DIRECTION ( 'NONE',  ( 0.8660254037842058938, 0.5000000000004030110, -5.443078266503040078E-12 ) ) ;
#9166=( NAMED_UNIT ( * ) SI_UNIT ( $, .STERADIAN. ) SOLID_ANGLE_UNIT ( ) );
#9185=ORIENTED_EDGE ( 'NONE', *, *, #1329, .F. ) ;
#9195=AXIS2_PLACEMENT_3D ( 'NONE', #4251, #13490, #18540 ) ;
#9216=ORIENTED_EDGE ( 'NONE', *, *, #16303, .T. ) ;
#9244=ORIENTED_EDGE ( 'NONE', *, *, #11432, .F. ) ;
#9264=CYLINDRICAL_SURFACE ( 'NONE', #19728, 0.3809999999999924558 ) ;
#9281=ORIENTED_EDGE ( 'NONE', *, *, #18736, .T. ) ;
#9285=SHAPE_REPRESENTATION_RELATIONSHIP ( 'NONE' , 'NONE' ,  #21348, #19727 ) ;
#9298=ORIENTED_EDGE ( 'NONE', *, *, #4227, .F. ) ;
#9324=DIRECTION ( 'NONE',  ( -2.324635735433000053E-14, 2.336881798971000105E-14, -1.000000000000000000 ) ) ;
#9351=ORIENTED_EDGE ( 'NONE', *, *, #14592, .F. ) ;
#9365=EDGE_CURVE ( 'NONE', #452, #1809, #15913, .T. ) ;
#9369=ORIENTED_EDGE ( 'NONE', *, *, #15029, .T. ) ;
#9394=EDGE_CURVE ( 'NONE', #10901, #14851, #21257, .T. ) ;
#9404=CARTESIAN_POINT ( 'NONE',  ( 142.0316867971999955, -3580.841199999999844, 2242.820000000000164 ) ) ;
#9447=CARTESIAN_POINT ( 'NONE',  ( 139.6999999999999886, -3576.320000000000164, 2245.359999999999673 ) ) ;
#9490=AXIS2_PLACEMENT_3D ( 'NONE', #5256, #14597, #3923 ) ;
#9497=DIRECTION ( 'NONE',  ( 5.432398939370942693E-28, 1.000000000000000000, 2.336881798971000105E-14 ) ) ;
#9518=VERTEX_POINT ( 'NONE', #14738 ) ;
#9553=DIRECTION ( 'NONE',  ( -0.8660254037817188832, 0.5000000000047110094, 3.181634500920069822E-14 ) ) ;
#9641=DIRECTION ( 'NONE',  ( -2.639068250487999990E-12, 1.000000000000000000, 0.000000000000000000 ) ) ;
#9643=ORIENTED_EDGE ( 'NONE', *, *, #20844, .T. ) ;
#9664=FACE_OUTER_BOUND ( 'NONE', #20791, .T. ) ;
#9700=CARTESIAN_POINT ( 'NONE',  ( 137.2104978356084075, -3580.932314744983614, 2239.009999999967931 ) ) ;
#9723=ORIENTED_EDGE ( 'NONE', *, *, #11514, .F. ) ;
#9741=ORIENTED_EDGE ( 'NONE', *, *, #3799, .F. ) ;
#9751=DIRECTION ( 'NONE',  ( 0.000000000000000000, 0.000000000000000000, 1.000000000000000000 ) ) ;
#9802=TOROIDAL_SURFACE ( 'NONE', #8329, 5.080000000000000071, 0.3810000000000000053 ) ;
#9830=AXIS2_PLACEMENT_3D ( 'NONE', #6326, #16969, #4440 ) ;
#9934=DIRECTION ( 'NONE',  ( 0.000000000000000000, -1.000000000000000000, 0.000000000000000000 ) ) ;
#9991=CARTESIAN_POINT ( 'NONE',  ( 139.6999999999999886, -3579.494999999999891, 2239.391000000000076 ) ) ;
#10010=CARTESIAN_POINT ( 'NONE',  ( 139.7000000000063835, -3576.802599999938593, 2239.391000000000076 ) ) ;
#10025=CIRCLE ( 'NONE', #19381, 3.175000000000149925 ) ;
#10042=ORIENTED_EDGE ( 'NONE', *, *, #16554, .T. ) ;
#10064=ORIENTED_EDGE ( 'NONE', *, *, #631, .F. ) ;
#10090=DIRECTION ( 'NONE',  ( 6.119339505807659940E-14, -1.000000000000000000, 0.000000000000000000 ) ) ;
#10107=ADVANCED_FACE ( 'NONE', ( #21791, #5755 ), #12886, .F. ) ;
#10119=ORIENTED_EDGE ( 'NONE', *, *, #17963, .F. ) ;
#10201=EDGE_LOOP ( 'NONE', ( #14060, #15783, #19384, #668 ) ) ;
#10319=CARTESIAN_POINT ( 'NONE',  ( 144.7800000000000011, -3579.494999999999891, 2244.978999999999814 ) ) ;
#10415=ORIENTED_EDGE ( 'NONE', *, *, #16303, .F. ) ;
#10425=ORIENTED_EDGE ( 'NONE', *, *, #22294, .T. ) ;
#10504=DIRECTION ( 'NONE',  ( 1.000000000000000000, 0.000000000000000000, 0.000000000000000000 ) ) ;
#10521=CARTESIAN_POINT ( 'NONE',  ( 139.6999999999999886, -3584.956000000000131, 2244.978999999999814 ) ) ;
#10526=PLANE ( 'NONE',  #3128 ) ;
#10554=AXIS2_PLACEMENT_3D ( 'NONE', #5744, #12877, #9016 ) ;
#10560=ORIENTED_EDGE ( 'NONE', *, *, #503, .T. ) ;
#10577=EDGE_CURVE ( 'NONE', #6733, #20297, #3912, .T. ) ;
#10592=ORIENTED_EDGE ( 'NONE', *, *, #9365, .F. ) ;
#10597=DIRECTION ( 'NONE',  ( -0.8660254037839826280, -0.5000000000007898127, 0.000000000000000000 ) ) ;
#10613=DIRECTION ( 'NONE',  ( 0.000000000000000000, 0.000000000000000000, -1.000000000000000000 ) ) ;
#10634=PLANE ( 'NONE',  #14492 ) ;
#10648=ORIENTED_EDGE ( 'NONE', *, *, #9394, .F. ) ;
#10665=CARTESIAN_POINT ( 'NONE',  ( 139.6999999999999886, -3579.494999999999891, 2245.359999999999673 ) ) ;
#10671=CYLINDRICAL_SURFACE ( 'NONE', #21883, 0.3809999999999180154 ) ;
#10712=DIRECTION ( 'NONE',  ( -2.848935406719999894E-12, 1.000000000000000000, 2.336881798978000141E-14 ) ) ;
#10743=FACE_OUTER_BOUND ( 'NONE', #812, .T. ) ;
#10771=DIRECTION ( 'NONE',  ( -0.5000000000031962211, 0.8660254037825932949, 0.000000000000000000 ) ) ;
#10783=EDGE_CURVE ( 'NONE', #20178, #3840, #1810, .T. ) ;
#10894=LINE ( 'NONE', #245, #11958 ) ;
#10901=VERTEX_POINT ( 'NONE', #1032 ) ;
#10964=DIRECTION ( 'NONE',  ( 0.000000000000000000, -1.000000000000000000, 0.000000000000000000 ) ) ;
#11005=ORIENTED_EDGE ( 'NONE', *, *, #9394, .T. ) ;
#11007=( BOUNDED_CURVE ( )  B_SPLINE_CURVE ( 3, ( #5971, #897, #9700, #14877 ),
 .UNSPECIFIED., .F., .T. ) 
 B_SPLINE_CURVE_WITH_KNOTS ( ( 4, 4 ),
 ( -9.769962616701377556E-15, 1.570796326937976328 ),
 .UNSPECIFIED. ) 
 CURVE ( )  GEOMETRIC_REPRESENTATION_ITEM ( )  RATIONAL_B_SPLINE_CURVE ( ( 1.000000000000000000, 0.8047378540906384714, 0.8047378540906384714, 1.000000000000000000 ) ) 
 REPRESENTATION_ITEM ( '' )  );
#11051=ORIENTED_EDGE ( 'NONE', *, *, #19383, .F. ) ;
#11096=EDGE_CURVE ( 'NONE', #6733, #13716, #8894, .T. ) ;
#11142=DIRECTION ( 'NONE',  ( 0.000000000000000000, -1.000000000000000000, 0.000000000000000000 ) ) ;
#11177=DIRECTION ( 'NONE',  ( 0.000000000000000000, -1.000000000000000000, 0.000000000000000000 ) ) ;
#11226=PRODUCT_DEFINITION ( 'UNKNOWN', '', #20249, #570 ) ;
#11272=CARTESIAN_POINT ( 'NONE',  ( 139.6999999999999886, -3574.034000000000106, 2245.359999999999673 ) ) ;
#11361=DIRECTION ( 'NONE',  ( -2.324635735433000053E-14, 0.000000000000000000, -1.000000000000000000 ) ) ;
#11378=LINE ( 'NONE', #12797, #22147 ) ;
#11392=EDGE_LOOP ( 'NONE', ( #361, #22976, #6603, #21800, #10648 ) ) ;
#11404=VECTOR ( 'NONE', #15460, 1000.000000000000000 ) ;
#11417=CIRCLE ( 'NONE', #9195, 1.904999999999823501 ) ;
#11432=EDGE_CURVE ( 'NONE', #309, #2778, #20059, .T. ) ;
#11441=EDGE_CURVE ( 'NONE', #21039, #1907, #907, .T. ) ;
#11442=LINE ( 'NONE', #2543, #19261 ) ;
#11445=AXIS2_PLACEMENT_3D ( 'NONE', #16573, #12947, #18332 ) ;
#11459=DIRECTION ( 'NONE',  ( -0.5000000000043488546, -0.8660254037819278272, 0.000000000000000000 ) ) ;
#11467=CARTESIAN_POINT ( 'NONE',  ( 142.4126867972053674, -3581.061170452544502, 2239.009999999999764 ) ) ;
#11498=AXIS2_PLACEMENT_3D ( 'NONE', #20692, #7822, #15085 ) ;
#11514=EDGE_CURVE ( 'NONE', #4556, #309, #23139, .T. ) ;
#11542=ADVANCED_FACE ( 'NONE', ( #12838 ), #5352, .T. ) ;
#11548=EDGE_CURVE ( 'NONE', #17616, #22650, #14030, .T. ) ;
#11556=CARTESIAN_POINT ( 'NONE',  ( 142.0316867971268096, -3580.841200000091249, 2239.391000000000076 ) ) ;
#11588=CARTESIAN_POINT ( 'NONE',  ( 144.7800000000000011, -3579.494999999999891, 2239.391000000000076 ) ) ;
#11610=VERTEX_POINT ( 'NONE', #7906 ) ;
#11649=ADVANCED_FACE ( 'NONE', ( #9664 ), #646, .F. ) ;
#11678=FACE_OUTER_BOUND ( 'NONE', #10201, .T. ) ;
#11746=( BOUNDED_CURVE ( )  B_SPLINE_CURVE ( 3, ( #20005, #18233, #16133, #2194 ),
 .UNSPECIFIED., .F., .T. ) 
 B_SPLINE_CURVE_WITH_KNOTS ( ( 4, 4 ),
 ( 1.570796326441848079, 3.141592653589783346 ),
 .UNSPECIFIED. ) 
 CURVE ( )  GEOMETRIC_REPRESENTATION_ITEM ( )  RATIONAL_B_SPLINE_CURVE ( ( 1.000000000000000000, 0.8047378540411529446, 0.8047378540411529446, 1.000000000000000000 ) ) 
 REPRESENTATION_ITEM ( '' )  );
#11770=AXIS2_PLACEMENT_3D ( 'NONE', #308, #9097, #14258 ) ;
#11773=CIRCLE ( 'NONE', #4666, 5.460999999999938126 ) ;
#11815=EDGE_CURVE ( 'NONE', #2778, #3685, #8037, .T. ) ;
#11857=ORIENTED_EDGE ( 'NONE', *, *, #20169, .F. ) ;
#11873=DIRECTION ( 'NONE',  ( 0.000000000000000000, -1.000000000000000000, 0.000000000000000000 ) ) ;
#11902=FACE_OUTER_BOUND ( 'NONE', #6994, .T. ) ;
#11906=ORIENTED_EDGE ( 'NONE', *, *, #21135, .T. ) ;
#11932=LINE ( 'NONE', #13579, #12979 ) ;
#11942=ORIENTED_EDGE ( 'NONE', *, *, #18146, .T. ) ;
#11958=VECTOR ( 'NONE', #3395, 1000.000000000000000 ) ;
#11968=CARTESIAN_POINT ( 'NONE',  ( 137.3683132029000262, -3578.148799999999937, 2239.391000000000076 ) ) ;
#11974=VERTEX_POINT ( 'NONE', #8315 ) ;
#11983=EDGE_CURVE ( 'NONE', #2593, #1809, #18854, .T. ) ;
#12011=PRODUCT_CONTEXT ( 'NONE', #15162, 'mechanical' ) ;
#12051=ORIENTED_EDGE ( 'NONE', *, *, #21056, .F. ) ;
#12265=DIRECTION ( 'NONE',  ( 0.000000000000000000, -1.000000000000000000, 0.000000000000000000 ) ) ;
#12268=LINE ( 'NONE', #3351, #16674 ) ;
#12341=ORIENTED_EDGE ( 'NONE', *, *, #3799, .T. ) ;
#12411=AXIS2_PLACEMENT_3D ( 'NONE', #18958, #3828, #14621 ) ;
#12413=AXIS2_PLACEMENT_3D ( 'NONE', #15727, #1651, #21000 ) ;
#12496=DIRECTION ( 'NONE',  ( 0.000000000000000000, 1.000000000000000000, 0.000000000000000000 ) ) ;
#12548=CARTESIAN_POINT ( 'NONE',  ( 139.6999999999999886, -3576.320000000000164, 2270.760000000000218 ) ) ;
#12567=CARTESIAN_POINT ( 'NONE',  ( 142.0316867971999955, -3580.841199999999844, 2242.820000000000164 ) ) ;
#12580=CARTESIAN_POINT ( 'NONE',  ( 142.4126867973300534, -3577.928829547225178, 2239.009999999999764 ) ) ;
#12593=EDGE_CURVE ( 'NONE', #1809, #118, #2319, .T. ) ;
#12645=ORIENTED_EDGE ( 'NONE', *, *, #16554, .F. ) ;
#12673=CARTESIAN_POINT ( 'NONE',  ( 142.4126867972053674, -3581.061170452544502, 2239.009999999999764 ) ) ;
#12681=EDGE_CURVE ( 'NONE', #14851, #10901, #22221, .T. ) ;
#12745=AXIS2_PLACEMENT_3D ( 'NONE', #15847, #17479, #8585 ) ;
#12760=CARTESIAN_POINT ( 'NONE',  ( 137.3683132029985927, -3578.148799999858966, 2239.391000000000076 ) ) ;
#12762=PRODUCT ( 'Screw 5', 'Screw 5', '', ( #12011 ) ) ;
#12776=CIRCLE ( 'NONE', #7908, 1.904999999999823501 ) ;
#12781=CARTESIAN_POINT ( 'NONE',  ( 139.6999999999999886, -3582.670000000000073, 2270.760000000000218 ) ) ;
#12797=CARTESIAN_POINT ( 'NONE',  ( 142.0316867971999955, -3580.841199999999844, 2242.820000000000164 ) ) ;
#12828=ADVANCED_FACE ( 'NONE', ( #10743 ), #18125, .T. ) ;
#12838=FACE_OUTER_BOUND ( 'NONE', #8514, .T. ) ;
#12842=CARTESIAN_POINT ( 'NONE',  ( 142.0316867971999955, -3578.148799999999937, 2239.391000000000076 ) ) ;
#12844=DIRECTION ( 'NONE',  ( 0.000000000000000000, 0.000000000000000000, 1.000000000000000000 ) ) ;
#12877=DIRECTION ( 'NONE',  ( -2.324635735433000053E-14, 2.336881798971000105E-14, -1.000000000000000000 ) ) ;
#12886=PLANE ( 'NONE',  #14821 ) ;
#12898=CARTESIAN_POINT ( 'NONE',  ( 139.6999999999999886, -3584.956000000000131, 2239.391000000000076 ) ) ;
#12909=ORIENTED_EDGE ( 'NONE', *, *, #17963, .T. ) ;
#12927=EDGE_CURVE ( 'NONE', #22190, #6461, #13415, .T. ) ;
#12929=DIRECTION ( 'NONE',  ( 2.324635735433000053E-14, 0.000000000000000000, 1.000000000000000000 ) ) ;
#12947=DIRECTION ( 'NONE',  ( -1.000000000000000000, -2.848935406719999894E-12, 0.000000000000000000 ) ) ;
#12979=VECTOR ( 'NONE', #19081, 1000.000000000000000 ) ;
#13009=ADVANCED_FACE ( 'NONE', ( #21974 ), #5940, .T. ) ;
#13011=CARTESIAN_POINT ( 'NONE',  ( 139.6999999999999886, -3574.034000000000106, 2244.978999999999814 ) ) ;
#13017=VECTOR ( 'NONE', #16313, 1000.000000000000000 ) ;
#13051=VERTEX_POINT ( 'NONE', #8727 ) ;
#13084=DIRECTION ( 'NONE',  ( 1.000000000000000000, 1.206643234470999950E-12, 0.000000000000000000 ) ) ;
#13101=EDGE_LOOP ( 'NONE', ( #9216, #8487, #9741, #7372, #6386, #5850 ) ) ;
#13123=VERTEX_POINT ( 'NONE', #22883 ) ;
#13139=DIRECTION ( 'NONE',  ( -0.8660254037824819395, -0.5000000000033889558, 5.608020032299880803E-12 ) ) ;
#13192=LINE ( 'NONE', #20237, #20648 ) ;
#13215=EDGE_CURVE ( 'NONE', #4556, #1232, #11773, .T. ) ;
#13216=CYLINDRICAL_SURFACE ( 'NONE', #1955, 0.3809999999998149867 ) ;
#13258=ORIENTED_EDGE ( 'NONE', *, *, #10577, .F. ) ;
#13372=MANIFOLD_SOLID_BREP ( 'TORNILLO1[1]', #18098 ) ;
#13376=ADVANCED_FACE ( 'NONE', ( #395 ), #2039, .T. ) ;
#13415=LINE ( 'NONE', #7803, #2422 ) ;
#13466=CARTESIAN_POINT ( 'NONE',  ( 137.3683132029000262, -3578.148799999999937, 2242.820000000000164 ) ) ;
#13490=DIRECTION ( 'NONE',  ( 0.000000000000000000, 0.000000000000000000, 1.000000000000000000 ) ) ;
#13508=DIRECTION ( 'NONE',  ( 1.000000000000000000, 0.000000000000000000, 0.000000000000000000 ) ) ;
#13567=CARTESIAN_POINT ( 'NONE',  ( 142.0316867971999955, -3578.148799999999937, 2242.820000000000164 ) ) ;
#13579=CARTESIAN_POINT ( 'NONE',  ( 139.7000000001000046, -3576.802599999999984, 2242.820000000000164 ) ) ;
#13584=ORIENTED_EDGE ( 'NONE', *, *, #11432, .T. ) ;
#13673=DIRECTION ( 'NONE',  ( 0.000000000000000000, 0.000000000000000000, 1.000000000000000000 ) ) ;
#13716=VERTEX_POINT ( 'NONE', #12673 ) ;
#13742=FACE_OUTER_BOUND ( 'NONE', #23122, .T. ) ;
#13761=VECTOR ( 'NONE', #3829, 1000.000000000000000 ) ;
#13762=ORIENTED_EDGE ( 'NONE', *, *, #12927, .F. ) ;
#13771=LINE ( 'NONE', #23002, #14832 ) ;
#13817=CARTESIAN_POINT ( 'NONE',  ( 139.6999999999999886, -3579.494999999999891, 2239.391000000000076 ) ) ;
#13859=( GEOMETRIC_REPRESENTATION_CONTEXT ( 3 ) GLOBAL_UNCERTAINTY_ASSIGNED_CONTEXT ( ( #4088 ) ) GLOBAL_UNIT_ASSIGNED_CONTEXT ( ( #16644, #4115, #9166 ) ) REPRESENTATION_CONTEXT ( 'NONE', 'WORKASPACE' ) );
#13903=VECTOR ( 'NONE', #9641, 1000.000000000000000 ) ;
#13969=DIRECTION ( 'NONE',  ( 1.298916404569000195E-12, -1.000000000000000000, 0.000000000000000000 ) ) ;
#13995=EDGE_CURVE ( 'NONE', #6733, #4557, #11746, .T. ) ;
#14030=CIRCLE ( 'NONE', #16269, 5.460999999999938126 ) ;
#14060=ORIENTED_EDGE ( 'NONE', *, *, #12927, .T. ) ;
#14132=ORIENTED_EDGE ( 'NONE', *, *, #17845, .F. ) ;
#14176=ORIENTED_EDGE ( 'NONE', *, *, #12681, .T. ) ;
#14252=EDGE_LOOP ( 'NONE', ( #4916, #9369, #2153, #21331 ) ) ;
#14258=DIRECTION ( 'NONE',  ( 0.000000000000000000, -1.000000000000000000, 0.000000000000000000 ) ) ;
#14293=DIRECTION ( 'NONE',  ( 0.000000000000000000, 1.000000000000000000, 0.000000000000000000 ) ) ;
#14362=ORIENTED_EDGE ( 'NONE', *, *, #15310, .T. ) ;
#14369=AXIS2_PLACEMENT_3D ( 'NONE', #10319, #5285, #15947 ) ;
#14492=AXIS2_PLACEMENT_3D ( 'NONE', #7249, #8770, #21425 ) ;
#14531=ADVANCED_FACE ( 'NONE', ( #16899 ), #6370, .T. ) ;
#14584=DIRECTION ( 'NONE',  ( -0.8660254037817188832, 0.5000000000047110094, 0.000000000000000000 ) ) ;
#14592=EDGE_CURVE ( 'NONE', #11974, #15124, #22194, .T. ) ;
#14597=DIRECTION ( 'NONE',  ( 2.324635735433000053E-14, 0.000000000000000000, 1.000000000000000000 ) ) ;
#14621=DIRECTION ( 'NONE',  ( 0.000000000000000000, 0.000000000000000000, -1.000000000000000000 ) ) ;
#14642=FACE_OUTER_BOUND ( 'NONE', #21230, .T. ) ;
#14738=CARTESIAN_POINT ( 'NONE',  ( 139.6999999999999886, -3577.590000000000146, 2272.030000000000200 ) ) ;
#14821=AXIS2_PLACEMENT_3D ( 'NONE', #20046, #8910, #7157 ) ;
#14829=CARTESIAN_POINT ( 'NONE',  ( 139.6999999999986528, -3582.187400000082107, 2239.391000000000076 ) ) ;
#14832=VECTOR ( 'NONE', #10597, 1000.000000000000000 ) ;
#14851=VERTEX_POINT ( 'NONE', #21700 ) ;
#14876=VECTOR ( 'NONE', #4460, 1000.000000000000000 ) ;
#14877=CARTESIAN_POINT ( 'NONE',  ( 136.9873132028999976, -3581.061170452877832, 2239.009999999999764 ) ) ;
#14937=ORIENTED_EDGE ( 'NONE', *, *, #3636, .T. ) ;
#14962=DIRECTION ( 'NONE',  ( -1.206643234470999950E-12, 1.000000000000000000, 0.000000000000000000 ) ) ;
#14982=ORIENTED_EDGE ( 'NONE', *, *, #1540, .F. ) ;
#14984=VECTOR ( 'NONE', #19364, 1000.000000000000114 ) ;
#15029=EDGE_CURVE ( 'NONE', #22190, #3892, #11007, .T. ) ;
#15037=DIRECTION ( 'NONE',  ( 0.000000000000000000, 0.000000000000000000, 1.000000000000000000 ) ) ;
#15085=DIRECTION ( 'NONE',  ( 0.000000000000000000, -1.000000000000000000, 0.000000000000000000 ) ) ;
#15106=ADVANCED_FACE ( 'NONE', ( #11678 ), #13216, .T. ) ;
#15109=CARTESIAN_POINT ( 'NONE',  ( 142.1895021644336339, -3580.932314744887208, 2239.010000000037508 ) ) ;
#15124=VERTEX_POINT ( 'NONE', #15214 ) ;
#15148=DIRECTION ( 'NONE',  ( 0.000000000000000000, -1.000000000000000000, 4.457650181899999573E-12 ) ) ;
#15150=ADVANCED_FACE ( 'NONE', ( #6430 ), #4317, .T. ) ;
#15162=APPLICATION_CONTEXT ( 'configuration controlled 3d designs of mechanical parts and assemblies' ) ;
#15209=CARTESIAN_POINT ( 'NONE',  ( 139.6999999999999886, -3582.670000000000073, 2270.760000000000218 ) ) ;
#15214=CARTESIAN_POINT ( 'NONE',  ( 144.7800000000000011, -3579.494999999999891, 2245.359999999999673 ) ) ;
#15237=ADVANCED_FACE ( 'NONE', ( #15442 ), #8327, .T. ) ;
#15264=AXIS2_PLACEMENT_3D ( 'NONE', #17138, #22520, #13508 ) ;
#15268=DIRECTION ( 'NONE',  ( 1.000000000000000000, 2.331176954593550859E-12, 0.000000000000000000 ) ) ;
#15272=DIRECTION ( 'NONE',  ( 0.000000000000000000, 0.000000000000000000, -1.000000000000000000 ) ) ;
#15310=EDGE_CURVE ( 'NONE', #21039, #9518, #16515, .T. ) ;
#15400=CIRCLE ( 'NONE', #6041, 0.3809999999999647002 ) ;
#15432=VERTEX_POINT ( 'NONE', #17775 ) ;
#15442=FACE_OUTER_BOUND ( 'NONE', #18863, .T. ) ;
#15460=DIRECTION ( 'NONE',  ( -2.185478394939000111E-13, -2.590196616223999907E-13, -1.000000000000000000 ) ) ;
#15514=EDGE_LOOP ( 'NONE', ( #1323, #19236, #10415, #18489 ) ) ;
#15519=EDGE_CURVE ( 'NONE', #2778, #10901, #15400, .T. ) ;
#15573=FACE_OUTER_BOUND ( 'NONE', #20950, .T. ) ;
#15631=CIRCLE ( 'NONE', #11498, 1.269999999999882334 ) ;
#15654=EDGE_LOOP ( 'NONE', ( #22444, #23039, #16278, #20501 ) ) ;
#15723=CARTESIAN_POINT ( 'NONE',  ( 136.9873132030508600, -3577.928829547506666, 2239.009999999999764 ) ) ;
#15727=CARTESIAN_POINT ( 'NONE',  ( 137.3683132029000262, -3580.841199999999844, 2242.820000000000164 ) ) ;
#15766=ADVANCED_FACE ( 'NONE', ( #11902 ), #19051, .T. ) ;
#15783=ORIENTED_EDGE ( 'NONE', *, *, #1191, .T. ) ;
#15784=CARTESIAN_POINT ( 'NONE',  ( 137.3683132029985927, -3578.148799999858966, 2239.391000000000076 ) ) ;
#15792=DIRECTION ( 'NONE',  ( -2.324635735433000053E-14, 2.336881798971000105E-14, -1.000000000000000000 ) ) ;
#15847=CARTESIAN_POINT ( 'NONE',  ( 139.6999999999999886, -3579.494999999999891, 2245.359999999999673 ) ) ;
#15913=LINE ( 'NONE', #19893, #13761 ) ;
#15918=AXIS2_PLACEMENT_3D ( 'NONE', #1067, #19121, #10090 ) ;
#15922=FACE_BOUND ( 'NONE', #8266, .T. ) ;
#15933=EDGE_LOOP ( 'NONE', ( #1506, #13584, #16854, #470, #14982 ) ) ;
#15947=DIRECTION ( 'NONE',  ( 0.000000000000000000, 0.000000000000000000, 1.000000000000000000 ) ) ;
#15953=DIRECTION ( 'NONE',  ( -0.8660254037840939834, -0.5000000000005969669, 0.000000000000000000 ) ) ;
#15961=CARTESIAN_POINT ( 'NONE',  ( 145.1609999999999729, -3579.494999999999891, 2244.978999999999814 ) ) ;
#16010=DIRECTION ( 'NONE',  ( 0.000000000000000000, 0.000000000000000000, 1.000000000000000000 ) ) ;
#16094=ORIENTED_EDGE ( 'NONE', *, *, #1080, .F. ) ;
#16098=DIRECTION ( 'NONE',  ( 1.224646799141920914E-16, -1.000000000000000000, -2.336881798971000421E-14 ) ) ;
#16122=EDGE_CURVE ( 'NONE', #3685, #13123, #3064, .T. ) ;
#16133=CARTESIAN_POINT ( 'NONE',  ( 142.0316867971961869, -3578.148799999863513, 2239.167815367201456 ) ) ;
#16162=ORIENTED_EDGE ( 'NONE', *, *, #13215, .F. ) ;
#16216=CARTESIAN_POINT ( 'NONE',  ( 139.6999999999999886, -3579.494999999999891, 2244.978999999999814 ) ) ;
#16269=AXIS2_PLACEMENT_3D ( 'NONE', #16464, #19875, #10964 ) ;
#16273=ORIENTED_EDGE ( 'NONE', *, *, #343, .T. ) ;
#16278=ORIENTED_EDGE ( 'NONE', *, *, #1116, .T. ) ;
#16288=DIRECTION ( 'NONE',  ( 1.206643234470999950E-12, -1.000000000000000000, -2.336881798973999985E-14 ) ) ;
#16295=AXIS2_PLACEMENT_3D ( 'NONE', #23115, #16098, #46 ) ;
#16303=EDGE_CURVE ( 'NONE', #3840, #11610, #11378, .T. ) ;
#16313=DIRECTION ( 'NONE',  ( -1.711270818677000004E-12, 1.000000000000000000, -3.793660610079000032E-12 ) ) ;
#16351=FACE_OUTER_BOUND ( 'NONE', #20684, .T. ) ;
#16392=ADVANCED_FACE ( 'NONE', ( #493 ), #9802, .T. ) ;
#16421=ORIENTED_EDGE ( 'NONE', *, *, #343, .F. ) ;
#16464=CARTESIAN_POINT ( 'NONE',  ( 139.6999999999999886, -3579.494999999999891, 2244.978999999999814 ) ) ;
#16515=CIRCLE ( 'NONE', #12411, 1.269999999999882334 ) ;
#16544=DIRECTION ( 'NONE',  ( 0.000000000000000000, 0.000000000000000000, -1.000000000000000000 ) ) ;
#16553=VECTOR ( 'NONE', #8995, 1000.000000000000227 ) ;
#16554=EDGE_CURVE ( 'NONE', #15432, #13716, #1966, .T. ) ;
#16573=CARTESIAN_POINT ( 'NONE',  ( 142.0316867971999955, -3580.841199999999844, 2242.820000000000164 ) ) ;
#16639=ORIENTED_EDGE ( 'NONE', *, *, #16122, .F. ) ;
#16644=( LENGTH_UNIT ( ) NAMED_UNIT ( * ) SI_UNIT ( .MILLI., .METRE. ) );
#16674=VECTOR ( 'NONE', #8868, 1000.000000000000000 ) ;
#16693=DIRECTION ( 'NONE',  ( 0.000000000000000000, -1.000000000000000000, 0.000000000000000000 ) ) ;
#16718=EDGE_CURVE ( 'NONE', #11610, #6461, #13192, .T. ) ;
#16741=UNCERTAINTY_MEASURE_WITH_UNIT (LENGTH_MEASURE( 1.000000000000000082E-05 ), #21126, 'distance_accuracy_value', 'NONE');
#16792=AXIS2_PLACEMENT_3D ( 'NONE', #16836, #20149, #890 ) ;
#16836=CARTESIAN_POINT ( 'NONE',  ( 139.6999999999999886, -3579.494999999999891, 2244.978999999999814 ) ) ;
#16854=ORIENTED_EDGE ( 'NONE', *, *, #15519, .T. ) ;
#16899=FACE_OUTER_BOUND ( 'NONE', #19702, .T. ) ;
#16969=DIRECTION ( 'NONE',  ( 0.8660254037825932949, 0.5000000000031962211, 0.000000000000000000 ) ) ;
#16974=LINE ( 'NONE', #2570, #18534 ) ;
#17014=CARTESIAN_POINT ( 'NONE',  ( 139.6999999999999886, -3579.494999999999891, 2245.359999999999673 ) ) ;
#17033=CARTESIAN_POINT ( 'NONE',  ( 139.7000000002929596, -3576.362659094888386, 2239.009999999999764 ) ) ;
#17103=CARTESIAN_POINT ( 'NONE',  ( 134.2390000000000043, -3579.494999999999891, 2239.391000000000076 ) ) ;
#17138=CARTESIAN_POINT ( 'NONE',  ( 139.6999999999999886, -3579.494999999999891, 2239.009999999999764 ) ) ;
#17246=EDGE_CURVE ( 'NONE', #17616, #3685, #6011, .T. ) ;
#17266=CARTESIAN_POINT ( 'NONE',  ( 139.7000000000068383, -3576.620370510379416, 2239.010000000095715 ) ) ;
#17279=AXIS2_PLACEMENT_3D ( 'NONE', #17798, #7145, #14293 ) ;
#17286=( BOUNDED_CURVE ( )  B_SPLINE_CURVE ( 3, ( #11467, #15109, #22235, #6208 ),
 .UNSPECIFIED., .F., .F. ) 
 B_SPLINE_CURVE_WITH_KNOTS ( ( 4, 4 ),
 ( 1.570796326964730927, 3.141592653589766471 ),
 .UNSPECIFIED. ) 
 CURVE ( )  GEOMETRIC_REPRESENTATION_ITEM ( )  RATIONAL_B_SPLINE_CURVE ( ( 1.000000000000000000, 0.8047378541644016892, 0.8047378541644016892, 1.000000000000000000 ) ) 
 REPRESENTATION_ITEM ( '' )  );
#17301=ORIENTED_EDGE ( 'NONE', *, *, #7508, .T. ) ;
#17306=VECTOR ( 'NONE', #16544, 1000.000000000000000 ) ;
#17309=ORIENTED_EDGE ( 'NONE', *, *, #11815, .F. ) ;
#17345=LINE ( 'NONE', #11968, #23009 ) ;
#17402=DIRECTION ( 'NONE',  ( -2.324635735433000053E-14, 0.000000000000000000, -1.000000000000000000 ) ) ;
#17406=VERTEX_POINT ( 'NONE', #22495 ) ;
#17437=CARTESIAN_POINT ( 'NONE',  ( 142.4126867972000241, -3577.928829547000078, 2239.009999999999764 ) ) ;
#17444=VECTOR ( 'NONE', #14584, 999.9999999999998863 ) ;
#17479=DIRECTION ( 'NONE',  ( 0.000000000000000000, -2.336881798971000105E-14, 1.000000000000000000 ) ) ;
#17498=CARTESIAN_POINT ( 'NONE',  ( 139.6999999999999886, -3579.494999999999891, 2239.391000000000076 ) ) ;
#17531=CARTESIAN_POINT ( 'NONE',  ( 137.3683132029000262, -3580.841199999999844, 2242.820000000000164 ) ) ;
#17547=CARTESIAN_POINT ( 'NONE',  ( 139.6999999999999886, -3579.494999999999891, 2239.009999999999764 ) ) ;
#17568=( BOUNDED_CURVE ( )  B_SPLINE_CURVE ( 3, ( #17033, #17266, #983, #10010 ),
 .UNSPECIFIED., .F., .T. ) 
 B_SPLINE_CURVE_WITH_KNOTS ( ( 4, 4 ),
 ( 1.570796327224941002, 3.141592653589829531 ),
 .UNSPECIFIED. ) 
 CURVE ( )  GEOMETRIC_REPRESENTATION_ITEM ( )  RATIONAL_B_SPLINE_CURVE ( ( 1.000000000000000000, 0.8047378542257188627, 0.8047378542257188627, 1.000000000000000000 ) ) 
 REPRESENTATION_ITEM ( '' )  );
#17616=VERTEX_POINT ( 'NONE', #13011 ) ;
#17654=CARTESIAN_POINT ( 'NONE',  ( 139.6999999999999886, -3579.494999999999891, 2244.978999999999814 ) ) ;
#17710=EDGE_CURVE ( 'NONE', #13716, #20178, #17286, .T. ) ;
#17731=DIRECTION ( 'NONE',  ( 1.000000000000000000, 5.432398939370942693E-28, -2.324635735433000053E-14 ) ) ;
#17752=ADVANCED_FACE ( 'NONE', ( #15573 ), #2672, .T. ) ;
#17775=CARTESIAN_POINT ( 'NONE',  ( 139.6999999997610757, -3582.627340905411984, 2239.009999999999764 ) ) ;
#17798=CARTESIAN_POINT ( 'NONE',  ( 139.6999999999999886, -3579.494999999999891, 2270.760000000000218 ) ) ;
#17821=CARTESIAN_POINT ( 'NONE',  ( 138.3436566013999993, -3577.145744321000166, 2239.391000000000076 ) ) ;
#17845=EDGE_CURVE ( 'NONE', #13123, #309, #7598, .T. ) ;
#17949=LINE ( 'NONE', #12567, #13017 ) ;
#17956=ADVANCED_FACE ( 'NONE', ( #15922, #2178 ), #10526, .T. ) ;
#17963=EDGE_CURVE ( 'NONE', #22650, #4556, #20349, .T. ) ;
#18003=APPLICATION_CONTEXT ( 'configuration controlled 3d designs of mechanical parts and assemblies' ) ;
#18014=AXIS2_PLACEMENT_3D ( 'NONE', #8389, #3571, #2047 ) ;
#18024=ORIENTED_EDGE ( 'NONE', *, *, #20844, .F. ) ;
#18034=CARTESIAN_POINT ( 'NONE',  ( 139.6999999999999886, -3582.187399999999798, 2242.820000000000164 ) ) ;
#18048=TOROIDAL_SURFACE ( 'NONE', #10554, 5.080000000000000071, 0.3810000000000000053 ) ;
#18078=AXIS2_PLACEMENT_3D ( 'NONE', #4478, #15272, #4259 ) ;
#18092=CARTESIAN_POINT ( 'NONE',  ( 142.0316867971999955, -3580.841199999999844, 2239.391000000000076 ) ) ;
#18098=CLOSED_SHELL ( 'NONE', ( #12828, #11542, #15237, #14531, #20699, #13376, #1126, #6408, #1718, #1204, #4670, #5843, #15150, #13009, #19400, #5545, #15106, #17752, #17956, #16392, #15766, #1831, #10107, #18971, #1799, #11649 ) ) ;
#18125=TOROIDAL_SURFACE ( 'NONE', #21128, 1.905000000000000027, 1.270000000000000018 ) ;
#18146=EDGE_CURVE ( 'NONE', #15124, #1232, #512, .T. ) ;
#18190=AXIS2_PLACEMENT_3D ( 'NONE', #8282, #13673, #777 ) ;
#18233=CARTESIAN_POINT ( 'NONE',  ( 142.1895021645321151, -3578.057685255049364, 2239.009999999921547 ) ) ;
#18251=ORIENTED_EDGE ( 'NONE', *, *, #11983, .T. ) ;
#18332=DIRECTION ( 'NONE',  ( -2.848935406719999894E-12, 1.000000000000000000, 0.000000000000000000 ) ) ;
#18352=CARTESIAN_POINT ( 'NONE',  ( 134.6199999999999761, -3579.494999999999891, 2239.391000000000076 ) ) ;
#18376=ORIENTED_EDGE ( 'NONE', *, *, #19383, .T. ) ;
#18379=DIRECTION ( 'NONE',  ( -0.8660254037817187722, 0.5000000000047108983, 0.000000000000000000 ) ) ;
#18489=ORIENTED_EDGE ( 'NONE', *, *, #10783, .F. ) ;
#18534=VECTOR ( 'NONE', #4671, 1000.000000000000114 ) ;
#18540=DIRECTION ( 'NONE',  ( 0.000000000000000000, 1.000000000000000000, 0.000000000000000000 ) ) ;
#18589=CARTESIAN_POINT ( 'NONE',  ( 137.3683132029000262, -3578.148799999999937, 2242.820000000000164 ) ) ;
#18650=ORIENTED_EDGE ( 'NONE', *, *, #11096, .F. ) ;
#18736=EDGE_CURVE ( 'NONE', #3892, #15432, #11442, .T. ) ;
#18854=LINE ( 'NONE', #13466, #11404 ) ;
#18863=EDGE_LOOP ( 'NONE', ( #9351, #9643, #12909, #8897, #19820 ) ) ;
#18880=VERTEX_POINT ( 'NONE', #6653 ) ;
#18958=CARTESIAN_POINT ( 'NONE',  ( 139.6999999999999886, -3577.590000000000146, 2270.760000000000218 ) ) ;
#18971=ADVANCED_FACE ( 'NONE', ( #6879 ), #21290, .T. ) ;
#19051=CYLINDRICAL_SURFACE ( 'NONE', #18014, 5.460999999999938126 ) ;
#19065=DIRECTION ( 'NONE',  ( 2.347365683444999541E-13, 0.000000000000000000, -1.000000000000000000 ) ) ;
#19081=DIRECTION ( 'NONE',  ( -6.475491540587999912E-14, 2.590196616235000036E-13, -1.000000000000000000 ) ) ;
#19121=DIRECTION ( 'NONE',  ( 0.000000000000000000, 0.000000000000000000, -1.000000000000000000 ) ) ;
#19236=ORIENTED_EDGE ( 'NONE', *, *, #16718, .F. ) ;
#19261=VECTOR ( 'NONE', #22209, 1000.000000000000114 ) ;
#19308=ORIENTED_EDGE ( 'NONE', *, *, #3188, .T. ) ;
#19319=CARTESIAN_POINT ( 'NONE',  ( 142.0316867971391162, -3578.148799999964467, 2239.391000000000076 ) ) ;
#19364=DIRECTION ( 'NONE',  ( 0.8660254037817868289, -0.5000000000045929927, -1.484475890920977686E-12 ) ) ;
#19381=AXIS2_PLACEMENT_3D ( 'NONE', #10665, #22958, #21573 ) ;
#19383=EDGE_CURVE ( 'NONE', #21039, #22822, #21113, .T. ) ;
#19384=ORIENTED_EDGE ( 'NONE', *, *, #18736, .F. ) ;
#19400=ADVANCED_FACE ( 'NONE', ( #16 ), #10671, .T. ) ;
#19490=ORIENTED_EDGE ( 'NONE', *, *, #12593, .T. ) ;
#19593=ORIENTED_EDGE ( 'NONE', *, *, #20313, .F. ) ;
#19679=EDGE_CURVE ( 'NONE', #6461, #20178, #16974, .T. ) ;
#19683=PRODUCT_DEFINITION_SHAPE ( 'NONE', 'NONE',  #11226 ) ;
#19702=EDGE_LOOP ( 'NONE', ( #20903, #4964, #17309, #9244, #9723, #10119 ) ) ;
#19727=ADVANCED_BREP_SHAPE_REPRESENTATION ( '', ( #13372, #5611 ), #13859 ) ;
#19728=AXIS2_PLACEMENT_3D ( 'NONE', #6928, #16288, #247 ) ;
#19768=CARTESIAN_POINT ( 'NONE',  ( 139.6999999999999886, -3579.494999999999891, 2270.760000000000218 ) ) ;
#19802=VECTOR ( 'NONE', #19065, 1000.000000000000000 ) ;
#19820=ORIENTED_EDGE ( 'NONE', *, *, #18146, .F. ) ;
#19871=PLANE ( 'NONE',  #11445 ) ;
#19875=DIRECTION ( 'NONE',  ( 2.324635735433000053E-14, 0.000000000000000000, 1.000000000000000000 ) ) ;
#19893=CARTESIAN_POINT ( 'NONE',  ( 139.7000000001000046, -3576.802599999999984, 2239.391000000000076 ) ) ;
#19911=AXIS2_PLACEMENT_3D ( 'NONE', #18034, #10771, #21556 ) ;
#19965=ORIENTED_EDGE ( 'NONE', *, *, #11983, .F. ) ;
#20004=CARTESIAN_POINT ( 'NONE',  ( 142.0316867971999955, -3578.148799999999937, 2242.820000000000164 ) ) ;
#20005=CARTESIAN_POINT ( 'NONE',  ( 142.4126867973300534, -3577.928829547225178, 2239.009999999999764 ) ) ;
#20018=PLANE ( 'NONE',  #5634 ) ;
#20046=CARTESIAN_POINT ( 'NONE',  ( 139.6999999999999886, -3579.494999999999891, 2245.359999999999673 ) ) ;
#20059=CIRCLE ( 'NONE', #23031, 5.460999999999938126 ) ;
#20112=CARTESIAN_POINT ( 'NONE',  ( 139.6999999999999886, -3584.956000000000131, 2245.359999999999673 ) ) ;
#20149=DIRECTION ( 'NONE',  ( 2.324635735433000053E-14, 0.000000000000000000, 1.000000000000000000 ) ) ;
#20169=EDGE_CURVE ( 'NONE', #1907, #21039, #20789, .T. ) ;
#20178=VERTEX_POINT ( 'NONE', #11556 ) ;
#20181=DIRECTION ( 'NONE',  ( 7.422379454680000104E-13, -1.000000000000000000, 4.288485907148999414E-12 ) ) ;
#20182=CARTESIAN_POINT ( 'NONE',  ( 139.6999999999999886, -3579.494999999999891, 2239.391000000000076 ) ) ;
#20222=CARTESIAN_POINT ( 'NONE',  ( 141.0563433985999779, -3577.145744321000166, 2239.391000000000076 ) ) ;
#20237=CARTESIAN_POINT ( 'NONE',  ( 139.6999999999999886, -3582.187399999999798, 2242.820000000000164 ) ) ;
#20249=PRODUCT_DEFINITION_FORMATION_WITH_SPECIFIED_SOURCE ( 'ANY', '', #12762, .NOT_KNOWN. ) ;
#20297=VERTEX_POINT ( 'NONE', #6887 ) ;
#20313=EDGE_CURVE ( 'NONE', #3892, #118, #12268, .T. ) ;
#20349=CIRCLE ( 'NONE', #9490, 5.460999999999938126 ) ;
#20501=ORIENTED_EDGE ( 'NONE', *, *, #13995, .F. ) ;
#20513=CARTESIAN_POINT ( 'NONE',  ( 139.6999999999999886, -3582.187399999999798, 2242.820000000000164 ) ) ;
#20640=TOROIDAL_SURFACE ( 'NONE', #17279, 1.905000000000000027, 1.270000000000000018 ) ;
#20648=VECTOR ( 'NONE', #22320, 1000.000000000000000 ) ;
#20670=CARTESIAN_POINT ( 'NONE',  ( 139.6999999999999886, -3581.400000000000091, 2272.030000000000200 ) ) ;
#20684=EDGE_LOOP ( 'NONE', ( #6336, #5190, #14937, #7832 ) ) ;
#20692=CARTESIAN_POINT ( 'NONE',  ( 139.6999999999999886, -3581.400000000000091, 2270.760000000000218 ) ) ;
#20699=ADVANCED_FACE ( 'NONE', ( #6854 ), #22618, .T. ) ;
#20759=AXIS2_PLACEMENT_3D ( 'NONE', #19768, #16010, #189 ) ;
#20774=CIRCLE ( 'NONE', #16295, 0.3809999999999647002 ) ;
#20789=CIRCLE ( 'NONE', #18190, 3.175000000000149925 ) ;
#20791=EDGE_LOOP ( 'NONE', ( #22452, #5205 ) ) ;
#20844=EDGE_CURVE ( 'NONE', #11974, #22650, #20774, .T. ) ;
#20886=ORIENTED_EDGE ( 'NONE', *, *, #17710, .F. ) ;
#20887=PLANE ( 'NONE',  #12413 ) ;
#20903=ORIENTED_EDGE ( 'NONE', *, *, #11548, .F. ) ;
#20950=EDGE_LOOP ( 'NONE', ( #4422, #20886, #12645, #3667 ) ) ;
#20958=DIRECTION ( 'NONE',  ( -2.324635735433000053E-14, 0.000000000000000000, -1.000000000000000000 ) ) ;
#21000=DIRECTION ( 'NONE',  ( 0.000000000000000000, 0.000000000000000000, -1.000000000000000000 ) ) ;
#21004=EDGE_CURVE ( 'NONE', #22946, #9518, #11417, .T. ) ;
#21039=VERTEX_POINT ( 'NONE', #3059 ) ;
#21056=EDGE_CURVE ( 'NONE', #1809, #22190, #17345, .T. ) ;
#21113=LINE ( 'NONE', #12548, #3172 ) ;
#21126=( LENGTH_UNIT ( ) NAMED_UNIT ( * ) SI_UNIT ( .MILLI., .METRE. ) );
#21128=AXIS2_PLACEMENT_3D ( 'NONE', #2298, #12844, #12496 ) ;
#21135=EDGE_CURVE ( 'NONE', #22822, #13051, #2089, .T. ) ;
#21220=ORIENTED_EDGE ( 'NONE', *, *, #22020, .F. ) ;
#21230=EDGE_LOOP ( 'NONE', ( #18024, #5857, #11942, #10425, #5027 ) ) ;
#21257=CIRCLE ( 'NONE', #15264, 5.080000000000000959 ) ;
#21258=ORIENTED_EDGE ( 'NONE', *, *, #9365, .T. ) ;
#21290=CYLINDRICAL_SURFACE ( 'NONE', #5416, 3.175000000000149925 ) ;
#21297=CARTESIAN_POINT ( 'NONE',  ( 137.3683132028983493, -3578.148799999801213, 2239.167815367371077 ) ) ;
#21331=ORIENTED_EDGE ( 'NONE', *, *, #12593, .F. ) ;
#21348=SHAPE_REPRESENTATION ( 'Screw 5', ( #5611 ), #13859 ) ;
#21425=DIRECTION ( 'NONE',  ( 0.000000000000000000, 0.000000000000000000, -1.000000000000000000 ) ) ;
#21510=VECTOR ( 'NONE', #3696, 1000.000000000000000 ) ;
#21556=DIRECTION ( 'NONE',  ( 0.000000000000000000, 0.000000000000000000, 1.000000000000000000 ) ) ;
#21573=DIRECTION ( 'NONE',  ( 6.119339505807659940E-14, -1.000000000000000000, 0.000000000000000000 ) ) ;
#21619=ORIENTED_EDGE ( 'NONE', *, *, #5406, .F. ) ;
#21669=FACE_OUTER_BOUND ( 'NONE', #15514, .T. ) ;
#21700=CARTESIAN_POINT ( 'NONE',  ( 144.7800000000000011, -3579.494999999999891, 2239.009999999999764 ) ) ;
#21791=FACE_BOUND ( 'NONE', #7919, .T. ) ;
#21800=ORIENTED_EDGE ( 'NONE', *, *, #1540, .T. ) ;
#21821=CARTESIAN_POINT ( 'NONE',  ( 137.3683132029000262, -3578.148799999999937, 2242.820000000000164 ) ) ;
#21883=AXIS2_PLACEMENT_3D ( 'NONE', #17821, #15953, #5291 ) ;
#21930=LINE ( 'NONE', #20513, #14876 ) ;
#21974=FACE_OUTER_BOUND ( 'NONE', #1948, .T. ) ;
#22020=EDGE_CURVE ( 'NONE', #20297, #118, #13771, .T. ) ;
#22075=CARTESIAN_POINT ( 'NONE',  ( 139.6999999999999886, -3579.494999999999891, 2272.030000000000200 ) ) ;
#22147=VECTOR ( 'NONE', #13139, 1000.000000000000227 ) ;
#22166=PLANE ( 'NONE',  #1171 ) ;
#22190=VERTEX_POINT ( 'NONE', #3615 ) ;
#22194=CIRCLE ( 'NONE', #8364, 5.080000000000000959 ) ;
#22209=DIRECTION ( 'NONE',  ( 0.8660254037820102058, -0.5000000000042060799, 0.000000000000000000 ) ) ;
#22221=CIRCLE ( 'NONE', #8393, 5.080000000000000959 ) ;
#22235=CARTESIAN_POINT ( 'NONE',  ( 142.0316867972038608, -3580.841200000134904, 2239.167815367294224 ) ) ;
#22294=EDGE_CURVE ( 'NONE', #1232, #17616, #4074, .T. ) ;
#22320=DIRECTION ( 'NONE',  ( 4.128125857098999856E-13, -1.295098308108999758E-13, -1.000000000000000000 ) ) ;
#22414=EDGE_CURVE ( 'NONE', #17406, #22190, #22797, .T. ) ;
#22444=ORIENTED_EDGE ( 'NONE', *, *, #11096, .T. ) ;
#22452=ORIENTED_EDGE ( 'NONE', *, *, #1080, .T. ) ;
#22495=CARTESIAN_POINT ( 'NONE',  ( 137.3683132029000262, -3580.841199999999844, 2242.820000000000164 ) ) ;
#22520=DIRECTION ( 'NONE',  ( 0.000000000000000000, 2.336881798971000105E-14, -1.000000000000000000 ) ) ;
#22547=EDGE_LOOP ( 'NONE', ( #10592, #9042, #9185, #18251 ) ) ;
#22617=VERTEX_POINT ( 'NONE', #20004 ) ;
#22618=TOROIDAL_SURFACE ( 'NONE', #6611, 5.080000000000000071, 0.3810000000000000053 ) ;
#22626=CARTESIAN_POINT ( 'NONE',  ( 139.6999999999986528, -3582.187400000179423, 2239.167815367220555 ) ) ;
#22650=VERTEX_POINT ( 'NONE', #1597 ) ;
#22747=CARTESIAN_POINT ( 'NONE',  ( 139.6999999997610757, -3582.627340905411984, 2239.009999999999764 ) ) ;
#22772=EDGE_LOOP ( 'NONE', ( #12051, #19965, #12341, #1867 ) ) ;
#22797=LINE ( 'NONE', #17531, #19802 ) ;
#22819=ORIENTED_EDGE ( 'NONE', *, *, #22294, .F. ) ;
#22822=VERTEX_POINT ( 'NONE', #9447 ) ;
#22858=CARTESIAN_POINT ( 'NONE',  ( 137.3683132029000262, -3578.148799999999937, 2242.820000000000164 ) ) ;
#22883=CARTESIAN_POINT ( 'NONE',  ( 145.1609999999999729, -3579.494999999999891, 2239.390999999999622 ) ) ;
#22946=VERTEX_POINT ( 'NONE', #20670 ) ;
#22958=DIRECTION ( 'NONE',  ( 0.000000000000000000, 0.000000000000000000, -1.000000000000000000 ) ) ;
#22976=ORIENTED_EDGE ( 'NONE', *, *, #11815, .T. ) ;
#23002=CARTESIAN_POINT ( 'NONE',  ( 139.7000000001000046, -3576.362659094999799, 2239.009999999999764 ) ) ;
#23009=VECTOR ( 'NONE', #13969, 1000.000000000000000 ) ;
#23031=AXIS2_PLACEMENT_3D ( 'NONE', #6534, #17402, #1359 ) ;
#23039=ORIENTED_EDGE ( 'NONE', *, *, #17710, .T. ) ;
#23094=( NAMED_UNIT ( * ) SI_UNIT ( $, .STERADIAN. ) SOLID_ANGLE_UNIT ( ) );
#23115=CARTESIAN_POINT ( 'NONE',  ( 134.6199999999999761, -3579.494999999999891, 2244.978999999999814 ) ) ;
#23122=EDGE_LOOP ( 'NONE', ( #13762, #4339, #1017, #2731 ) ) ;
#23139=LINE ( 'NONE', #20112, #21510 ) ;
#23142=CARTESIAN_POINT ( 'NONE',  ( 139.6999999999999886, -3579.494999999999891, 2239.009999999999764 ) ) ;
#23208=COLOUR_RGB('Black',0.12,0.14,0.17);
#23209=FILL_AREA_STYLE_COLOUR('',#23208);
#23210=FILL_AREA_STYLE('',(#23209));
#23211=SURFACE_STYLE_FILL_AREA(#23210);
#23212=SURFACE_SIDE_STYLE('',(#23211));
#23213=SURFACE_STYLE_USAGE(.BOTH.,#23212);
#23214=PRESENTATION_STYLE_ASSIGNMENT((#23213));
#23225=STYLED_ITEM('',(#23214),#13372);
#23237=MECHANICAL_DESIGN_GEOMETRIC_PRESENTATION_REPRESENTATION('',(#23225),#2257);
ENDSEC;
END-ISO-10303-21;
